ISO-10303-21;
HEADER;
FILE_DESCRIPTION (('STEP AP214'),
    '1' );
FILE_NAME ('Handle.step',
    '2026-10-28T16:39:03',
    ( '' ),
    ( '' ),
    'SwSTEP 2.0',
    'SolidWorks 2024',
    '' );
FILE_SCHEMA (( 'AUTOMOTIVE_DESIGN' ));
ENDSEC;

DATA;
#10=ADVANCED_BREP_SHAPE_REPRESENTATION ( '', ( #4174, #5785 ), #5126 ) ;
#54=LINE ( 'NONE', #4948, #4837 ) ;
#60=DIRECTION ( 'NONE',  ( 0.000000000000000000, -0.000000000000000000, 1.000000000000000000 ) ) ;
#71=DIRECTION ( 'NONE',  ( -0.000000000000000000, -0.000000000000000000, -1.000000000000000000 ) ) ;
#158=ORIENTED_EDGE ( 'NONE', *, *, #3995, .T. ) ;
#163=CARTESIAN_POINT ( 'NONE',  ( 412.5000000000001137, 1.530808498934191127E-15, 0.000000000000000000 ) ) ;
#184=EDGE_LOOP ( 'NONE', ( #4284, #4877, #609, #2812 ) ) ;
#208=CIRCLE ( 'NONE', #1871, 12.50000000000001066 ) ;
#245=CARTESIAN_POINT ( 'NONE',  ( 412.5000000000001137, 1.530808498934191916E-15, 25.00000000000000000 ) ) ;
#293=LINE ( 'NONE', #3268, #3948 ) ;
#299=DIRECTION ( 'NONE',  ( -1.000000000000000000, 0.000000000000000000, 0.000000000000000000 ) ) ;
#312=CARTESIAN_POINT ( 'NONE',  ( 400.0000000000000568, -25.00000000000000000, 0.000000000000000000 ) ) ;
#342=VERTEX_POINT ( 'NONE', #2510 ) ;
#345=VERTEX_POINT ( 'NONE', #4949 ) ;
#357=EDGE_LOOP ( 'NONE', ( #1319, #5356 ) ) ;
#467=FACE_BOUND ( 'NONE', #5993, .T. ) ;
#497=DIRECTION ( 'NONE',  ( 1.000000000000000000, 0.000000000000000000, 0.000000000000000000 ) ) ;
#552=LINE ( 'NONE', #3634, #2145 ) ;
#609=ORIENTED_EDGE ( 'NONE', *, *, #5693, .F. ) ;
#623=ADVANCED_FACE ( 'NONE', ( #7279, #3510, #467 ), #2915, .T. ) ;
#625=ADVANCED_FACE ( 'NONE', ( #1700 ), #4140, .F. ) ;
#654=DIRECTION ( 'NONE',  ( 1.000000000000000000, 0.000000000000000000, 0.000000000000000000 ) ) ;
#667=ORIENTED_EDGE ( 'NONE', *, *, #3236, .T. ) ;
#708=UNCERTAINTY_MEASURE_WITH_UNIT (LENGTH_MEASURE( 1.000000000000000082E-05 ), #6956, 'distance_accuracy_value', 'NONE');
#716=LINE ( 'NONE', #3209, #7756 ) ;
#719=ORIENTED_EDGE ( 'NONE', *, *, #6111, .F. ) ;
#720=( GEOMETRIC_REPRESENTATION_CONTEXT ( 3 ) GLOBAL_UNCERTAINTY_ASSIGNED_CONTEXT ( ( #708 ) ) GLOBAL_UNIT_ASSIGNED_CONTEXT ( ( #6956, #5552, #3868 ) ) REPRESENTATION_CONTEXT ( 'NONE', 'WORKASPACE' ) );
#799=ORIENTED_EDGE ( 'NONE', *, *, #5542, .T. ) ;
#806=LINE ( 'NONE', #1444, #7164 ) ;
#881=ADVANCED_FACE ( 'NONE', ( #6427 ), #5096, .F. ) ;
#935=ORIENTED_EDGE ( 'NONE', *, *, #5561, .F. ) ;
#938=CLOSED_SHELL ( 'NONE', ( #3259, #881, #6446, #623, #2835, #6205, #3362, #7832, #625, #4608, #4436 ) ) ;
#941=CARTESIAN_POINT ( 'NONE',  ( 387.5000000000000568, 0.000000000000000000, 25.00000000000000000 ) ) ;
#967=EDGE_CURVE ( 'NONE', #3100, #3167, #6092, .T. ) ;
#1063=EDGE_LOOP ( 'NONE', ( #6818, #5603, #2310, #5112 ) ) ;
#1088=CARTESIAN_POINT ( 'NONE',  ( 400.0000000000000568, 0.000000000000000000, 0.000000000000000000 ) ) ;
#1122=ORIENTED_EDGE ( 'NONE', *, *, #5838, .T. ) ;
#1213=AXIS2_PLACEMENT_3D ( 'NONE', #7802, #2313, #4744 ) ;
#1225=EDGE_LOOP ( 'NONE', ( #1493, #5646 ) ) ;
#1242=AXIS2_PLACEMENT_3D ( 'NONE', #1410, #4297, #6871 ) ;
#1253=VECTOR ( 'NONE', #2042, 1000.000000000000000 ) ;
#1267=ORIENTED_EDGE ( 'NONE', *, *, #4218, .T. ) ;
#1273=CARTESIAN_POINT ( 'NONE',  ( 0.000000000000000000, -25.00000000000000000, 25.00000000000000000 ) ) ;
#1319=ORIENTED_EDGE ( 'NONE', *, *, #7432, .F. ) ;
#1356=DIRECTION ( 'NONE',  ( 0.000000000000000000, 0.000000000000000000, 1.000000000000000000 ) ) ;
#1410=CARTESIAN_POINT ( 'NONE',  ( 350.0000000000001137, -6.123233995736758985E-15, 25.00000000000000000 ) ) ;
#1412=CARTESIAN_POINT ( 'NONE',  ( 400.0000000000000568, 0.000000000000000000, 25.00000000000000000 ) ) ;
#1418=CARTESIAN_POINT ( 'NONE',  ( 0.000000000000000000, -25.00000000000000000, 0.000000000000000000 ) ) ;
#1438=ORIENTED_EDGE ( 'NONE', *, *, #6023, .F. ) ;
#1444=CARTESIAN_POINT ( 'NONE',  ( 0.000000000000000000, 25.00000000000000000, 0.000000000000000000 ) ) ;
#1488=CIRCLE ( 'NONE', #6749, 25.00000000000000000 ) ;
#1493=ORIENTED_EDGE ( 'NONE', *, *, #4826, .T. ) ;
#1533=DIRECTION ( 'NONE',  ( 0.000000000000000000, 0.000000000000000000, 1.000000000000000000 ) ) ;
#1546=DIRECTION ( 'NONE',  ( -0.000000000000000000, -0.000000000000000000, -1.000000000000000000 ) ) ;
#1556=ORIENTED_EDGE ( 'NONE', *, *, #4165, .T. ) ;
#1558=ORIENTED_EDGE ( 'NONE', *, *, #5495, .T. ) ;
#1579=ORIENTED_EDGE ( 'NONE', *, *, #5495, .F. ) ;
#1599=AXIS2_PLACEMENT_3D ( 'NONE', #2483, #1356, #5654 ) ;
#1604=VECTOR ( 'NONE', #2925, 1000.000000000000000 ) ;
#1612=EDGE_CURVE ( 'NONE', #5578, #4376, #3391, .T. ) ;
#1626=( NAMED_UNIT ( * ) PLANE_ANGLE_UNIT ( ) SI_UNIT ( $, .RADIAN. ) );
#1633=CARTESIAN_POINT ( 'NONE',  ( -25.00000000000000000, 0.000000000000000000, 0.000000000000000000 ) ) ;
#1637=VERTEX_POINT ( 'NONE', #5602 ) ;
#1648=AXIS2_PLACEMENT_3D ( 'NONE', #3340, #2737, #2011 ) ;
#1669=ORIENTED_EDGE ( 'NONE', *, *, #4014, .F. ) ;
#1700=FACE_OUTER_BOUND ( 'NONE', #184, .T. ) ;
#1707=CARTESIAN_POINT ( 'NONE',  ( 350.0000000000001137, -6.123233995736758985E-15, 25.00000000000000000 ) ) ;
#1752=AXIS2_PLACEMENT_3D ( 'NONE', #5760, #3385, #7162 ) ;
#1764=CIRCLE ( 'NONE', #6769, 25.00000000000002132 ) ;
#1810=PRODUCT_DEFINITION_FORMATION_WITH_SPECIFIED_SOURCE ( 'ANY', '', #7704, .NOT_KNOWN. ) ;
#1871=AXIS2_PLACEMENT_3D ( 'NONE', #6161, #4993, #2549 ) ;
#1891=SHAPE_DEFINITION_REPRESENTATION ( #5269, #3730 ) ;
#1921=APPLICATION_CONTEXT ( 'automotive_design' ) ;
#1948=ORIENTED_EDGE ( 'NONE', *, *, #4383, .F. ) ;
#1956=CARTESIAN_POINT ( 'NONE',  ( 0.000000000000000000, 25.00000000000000000, 25.00000000000000000 ) ) ;
#1967=DIRECTION ( 'NONE',  ( 0.000000000000000000, 0.000000000000000000, 1.000000000000000000 ) ) ;
#1993=LINE ( 'NONE', #3738, #4666 ) ;
#2011=DIRECTION ( 'NONE',  ( 1.000000000000000000, 0.000000000000000000, 0.000000000000000000 ) ) ;
#2012=CARTESIAN_POINT ( 'NONE',  ( 0.000000000000000000, 0.000000000000000000, 0.000000000000000000 ) ) ;
#2023=DIRECTION ( 'NONE',  ( 1.000000000000000000, 0.000000000000000000, 0.000000000000000000 ) ) ;
#2028=FACE_OUTER_BOUND ( 'NONE', #3878, .T. ) ;
#2042=DIRECTION ( 'NONE',  ( -0.000000000000000000, -0.000000000000000000, -1.000000000000000000 ) ) ;
#2116=ORIENTED_EDGE ( 'NONE', *, *, #1612, .T. ) ;
#2123=PRODUCT_DEFINITION ( 'UNKNOWN', '', #1810, #4068 ) ;
#2143=VERTEX_POINT ( 'NONE', #7031 ) ;
#2145=VECTOR ( 'NONE', #6417, 1000.000000000000000 ) ;
#2168=DIRECTION ( 'NONE',  ( 1.000000000000000000, 0.000000000000000000, 0.000000000000000000 ) ) ;
#2214=CYLINDRICAL_SURFACE ( 'NONE', #7786, 12.50000000000001066 ) ;
#2303=CARTESIAN_POINT ( 'NONE',  ( 0.000000000000000000, 25.00000000000000000, 0.000000000000000000 ) ) ;
#2306=CIRCLE ( 'NONE', #3324, 12.50000000000001066 ) ;
#2310=ORIENTED_EDGE ( 'NONE', *, *, #4826, .F. ) ;
#2313=DIRECTION ( 'NONE',  ( 0.000000000000000000, 0.000000000000000000, 1.000000000000000000 ) ) ;
#2318=( NAMED_UNIT ( * ) SI_UNIT ( $, .STERADIAN. ) SOLID_ANGLE_UNIT ( ) );
#2351=DIRECTION ( 'NONE',  ( 1.000000000000000000, 0.000000000000000000, 0.000000000000000000 ) ) ;
#2381=LINE ( 'NONE', #4818, #4691 ) ;
#2391=CIRCLE ( 'NONE', #5848, 25.00000000000000000 ) ;
#2397=AXIS2_PLACEMENT_3D ( 'NONE', #5953, #7799, #7237 ) ;
#2410=ORIENTED_EDGE ( 'NONE', *, *, #2491, .F. ) ;
#2448=ORIENTED_EDGE ( 'NONE', *, *, #5214, .T. ) ;
#2483=CARTESIAN_POINT ( 'NONE',  ( 0.000000000000000000, 0.000000000000000000, 0.000000000000000000 ) ) ;
#2491=EDGE_CURVE ( 'NONE', #6165, #3100, #5823, .T. ) ;
#2510=CARTESIAN_POINT ( 'NONE',  ( 400.0000000000000568, -25.00000000000000000, 25.00000000000000000 ) ) ;
#2520=ORIENTED_EDGE ( 'NONE', *, *, #5693, .T. ) ;
#2544=EDGE_LOOP ( 'NONE', ( #6663, #1556 ) ) ;
#2549=DIRECTION ( 'NONE',  ( 1.000000000000000000, 0.000000000000000000, 0.000000000000000000 ) ) ;
#2556=UNCERTAINTY_MEASURE_WITH_UNIT (LENGTH_MEASURE( 1.000000000000000082E-05 ), #2962, 'distance_accuracy_value', 'NONE');
#2628=AXIS2_PLACEMENT_3D ( 'NONE', #2012, #4453, #5210 ) ;
#2639=ORIENTED_EDGE ( 'NONE', *, *, #5542, .F. ) ;
#2668=VECTOR ( 'NONE', #5915, 1000.000000000000000 ) ;
#2706=DIRECTION ( 'NONE',  ( -0.000000000000000000, -0.000000000000000000, -1.000000000000000000 ) ) ;
#2737=DIRECTION ( 'NONE',  ( 0.000000000000000000, 0.000000000000000000, 1.000000000000000000 ) ) ;
#2772=MECHANICAL_DESIGN_GEOMETRIC_PRESENTATION_REPRESENTATION('',(#6359),#720);
#2784=CIRCLE ( 'NONE', #3425, 12.50000000000001066 ) ;
#2792=ORIENTED_EDGE ( 'NONE', *, *, #967, .F. ) ;
#2798=CARTESIAN_POINT ( 'NONE',  ( 0.000000000000000000, 0.000000000000000000, 25.00000000000000000 ) ) ;
#2812=ORIENTED_EDGE ( 'NONE', *, *, #5620, .T. ) ;
#2815=CARTESIAN_POINT ( 'NONE',  ( 0.000000000000000000, 0.000000000000000000, 0.000000000000000000 ) ) ;
#2835=ADVANCED_FACE ( 'NONE', ( #3132, #6137, #4881 ), #6778, .F. ) ;
#2841=EDGE_CURVE ( 'NONE', #342, #3644, #1993, .T. ) ;
#2862=CARTESIAN_POINT ( 'NONE',  ( 0.000000000000000000, 0.000000000000000000, 25.00000000000000000 ) ) ;
#2889=ORIENTED_EDGE ( 'NONE', *, *, #2901, .T. ) ;
#2896=AXIS2_PLACEMENT_3D ( 'NONE', #1273, #6725, #60 ) ;
#2901=EDGE_CURVE ( 'NONE', #345, #3167, #716, .T. ) ;
#2915=PLANE ( 'NONE',  #1213 ) ;
#2924=ORIENTED_EDGE ( 'NONE', *, *, #5154, .F. ) ;
#2925=DIRECTION ( 'NONE',  ( 1.000000000000000000, 0.000000000000000000, 0.000000000000000000 ) ) ;
#2942=CIRCLE ( 'NONE', #1648, 12.50000000000001066 ) ;
#2962=( LENGTH_UNIT ( ) NAMED_UNIT ( * ) SI_UNIT ( .MILLI., .METRE. ) );
#2998=VERTEX_POINT ( 'NONE', #5194 ) ;
#3071=CARTESIAN_POINT ( 'NONE',  ( 400.0000000000000568, 25.00000000000000000, 0.000000000000000000 ) ) ;
#3100=VERTEX_POINT ( 'NONE', #1633 ) ;
#3104=DIRECTION ( 'NONE',  ( -1.000000000000000000, 0.000000000000000000, 0.000000000000000000 ) ) ;
#3132=FACE_OUTER_BOUND ( 'NONE', #5957, .T. ) ;
#3154=ORIENTED_EDGE ( 'NONE', *, *, #6118, .F. ) ;
#3167=VERTEX_POINT ( 'NONE', #6647 ) ;
#3209=CARTESIAN_POINT ( 'NONE',  ( 0.000000000000000000, -25.00000000000000000, 25.00000000000000000 ) ) ;
#3210=ORIENTED_EDGE ( 'NONE', *, *, #4383, .T. ) ;
#3236=EDGE_CURVE ( 'NONE', #345, #342, #4713, .T. ) ;
#3259=ADVANCED_FACE ( 'NONE', ( #4791 ), #7214, .F. ) ;
#3268=CARTESIAN_POINT ( 'NONE',  ( -25.00000000000000000, 0.000000000000000000, 25.00000000000000000 ) ) ;
#3300=DIRECTION ( 'NONE',  ( -1.000000000000000000, 0.000000000000000000, 0.000000000000000000 ) ) ;
#3324=AXIS2_PLACEMENT_3D ( 'NONE', #6149, #7537, #654 ) ;
#3340=CARTESIAN_POINT ( 'NONE',  ( 350.0000000000001137, -6.123233995736758985E-15, 0.000000000000000000 ) ) ;
#3362=ADVANCED_FACE ( 'NONE', ( #5259 ), #4270, .F. ) ;
#3385=DIRECTION ( 'NONE',  ( 0.000000000000000000, 0.000000000000000000, 1.000000000000000000 ) ) ;
#3386=CARTESIAN_POINT ( 'NONE',  ( 412.5000000000001137, 1.530808498934191127E-15, 25.00000000000000000 ) ) ;
#3391=CIRCLE ( 'NONE', #7234, 12.50000000000001066 ) ;
#3413=DIRECTION ( 'NONE',  ( 0.000000000000000000, 0.000000000000000000, 1.000000000000000000 ) ) ;
#3418=FACE_OUTER_BOUND ( 'NONE', #4797, .T. ) ;
#3425=AXIS2_PLACEMENT_3D ( 'NONE', #1088, #5984, #497 ) ;
#3456=DIRECTION ( 'NONE',  ( 1.000000000000000000, 0.000000000000000000, 0.000000000000000000 ) ) ;
#3510=FACE_OUTER_BOUND ( 'NONE', #3692, .T. ) ;
#3520=AXIS2_PLACEMENT_3D ( 'NONE', #3548, #5995, #4413 ) ;
#3548=CARTESIAN_POINT ( 'NONE',  ( 0.000000000000000000, 25.00000000000000000, 25.00000000000000000 ) ) ;
#3634=CARTESIAN_POINT ( 'NONE',  ( 337.5000000000000568, -6.123233995736758985E-15, 25.00000000000000000 ) ) ;
#3644=VERTEX_POINT ( 'NONE', #312 ) ;
#3692=EDGE_LOOP ( 'NONE', ( #4518, #1267, #667, #5100, #2520 ) ) ;
#3702=EDGE_LOOP ( 'NONE', ( #6853, #4757, #3740, #2889 ) ) ;
#3705=FACE_OUTER_BOUND ( 'NONE', #7210, .T. ) ;
#3730=SHAPE_REPRESENTATION ( 'Handle', ( #5785 ), #5126 ) ;
#3734=ORIENTED_EDGE ( 'NONE', *, *, #4427, .T. ) ;
#3738=CARTESIAN_POINT ( 'NONE',  ( 400.0000000000000568, -25.00000000000000000, 25.00000000000000000 ) ) ;
#3740=ORIENTED_EDGE ( 'NONE', *, *, #3236, .F. ) ;
#3757=DIRECTION ( 'NONE',  ( 0.000000000000000000, 0.000000000000000000, 1.000000000000000000 ) ) ;
#3824=AXIS2_PLACEMENT_3D ( 'NONE', #5994, #1967, #6115 ) ;
#3829=AXIS2_PLACEMENT_3D ( 'NONE', #2862, #4009, #6464 ) ;
#3868=( NAMED_UNIT ( * ) SI_UNIT ( $, .STERADIAN. ) SOLID_ANGLE_UNIT ( ) );
#3869=DIRECTION ( 'NONE',  ( 1.000000000000000000, 0.000000000000000000, 0.000000000000000000 ) ) ;
#3878=EDGE_LOOP ( 'NONE', ( #5073, #4018, #6779, #5652 ) ) ;
#3927=APPLICATION_CONTEXT ( 'automotive_design' ) ;
#3948=VECTOR ( 'NONE', #5180, 1000.000000000000000 ) ;
#3967=DIRECTION ( 'NONE',  ( 0.000000000000000000, 0.000000000000000000, 1.000000000000000000 ) ) ;
#3974=DIRECTION ( 'NONE',  ( 1.000000000000000000, 0.000000000000000000, 0.000000000000000000 ) ) ;
#3981=CARTESIAN_POINT ( 'NONE',  ( 400.0000000000000568, 25.00000000000000000, 25.00000000000000000 ) ) ;
#3995=EDGE_CURVE ( 'NONE', #4376, #5884, #5276, .T. ) ;
#4009=DIRECTION ( 'NONE',  ( -0.000000000000000000, -0.000000000000000000, -1.000000000000000000 ) ) ;
#4014=EDGE_CURVE ( 'NONE', #4926, #1637, #2391, .T. ) ;
#4018=ORIENTED_EDGE ( 'NONE', *, *, #5620, .F. ) ;
#4045=CARTESIAN_POINT ( 'NONE',  ( 400.0000000000000568, 0.000000000000000000, 25.00000000000000000 ) ) ;
#4068=PRODUCT_DEFINITION_CONTEXT ( 'detailed design', #3927, 'design' ) ;
#4074=DIRECTION ( 'NONE',  ( 0.000000000000000000, 0.000000000000000000, 1.000000000000000000 ) ) ;
#4102=CARTESIAN_POINT ( 'NONE',  ( 387.5000000000000568, 0.000000000000000000, 25.00000000000000000 ) ) ;
#4110=CARTESIAN_POINT ( 'NONE',  ( 0.000000000000000000, 0.000000000000000000, 0.000000000000000000 ) ) ;
#4140=PLANE ( 'NONE',  #3520 ) ;
#4154=DIRECTION ( 'NONE',  ( -1.000000000000000000, 0.000000000000000000, 0.000000000000000000 ) ) ;
#4165=EDGE_CURVE ( 'NONE', #5042, #2998, #208, .T. ) ;
#4174=MANIFOLD_SOLID_BREP ( 'Yükseklik-Ekstrüzyon1', #938 ) ;
#4184=EDGE_LOOP ( 'NONE', ( #2639, #1669, #3734, #7281 ) ) ;
#4186=DIRECTION ( 'NONE',  ( 0.000000000000000000, 0.000000000000000000, 1.000000000000000000 ) ) ;
#4218=EDGE_CURVE ( 'NONE', #1637, #345, #1488, .T. ) ;
#4237=ORIENTED_EDGE ( 'NONE', *, *, #2901, .F. ) ;
#4270=PLANE ( 'NONE',  #2896 ) ;
#4284=ORIENTED_EDGE ( 'NONE', *, *, #6111, .T. ) ;
#4297=DIRECTION ( 'NONE',  ( -0.000000000000000000, -0.000000000000000000, -1.000000000000000000 ) ) ;
#4321=EDGE_CURVE ( 'NONE', #4446, #5884, #5341, .T. ) ;
#4376=VERTEX_POINT ( 'NONE', #4102 ) ;
#4383=EDGE_CURVE ( 'NONE', #4671, #2143, #5980, .T. ) ;
#4394=DIRECTION ( 'NONE',  ( -0.000000000000000000, -0.000000000000000000, -1.000000000000000000 ) ) ;
#4406=AXIS2_PLACEMENT_3D ( 'NONE', #1412, #5790, #3300 ) ;
#4413=DIRECTION ( 'NONE',  ( 0.000000000000000000, -0.000000000000000000, -1.000000000000000000 ) ) ;
#4427=EDGE_CURVE ( 'NONE', #4926, #6165, #2381, .T. ) ;
#4436=ADVANCED_FACE ( 'NONE', ( #6191 ), #6752, .F. ) ;
#4446=VERTEX_POINT ( 'NONE', #163 ) ;
#4453=DIRECTION ( 'NONE',  ( 0.000000000000000000, 0.000000000000000000, 1.000000000000000000 ) ) ;
#4464=DIRECTION ( 'NONE',  ( 1.000000000000000000, 0.000000000000000000, 0.000000000000000000 ) ) ;
#4518=ORIENTED_EDGE ( 'NONE', *, *, #4014, .T. ) ;
#4535=DIRECTION ( 'NONE',  ( -1.000000000000000000, -0.000000000000000000, -0.000000000000000000 ) ) ;
#4608=ADVANCED_FACE ( 'NONE', ( #3418 ), #2214, .F. ) ;
#4610=DIRECTION ( 'NONE',  ( -0.000000000000000000, -0.000000000000000000, -1.000000000000000000 ) ) ;
#4618=LINE ( 'NONE', #5721, #7026 ) ;
#4624=ORIENTED_EDGE ( 'NONE', *, *, #4165, .F. ) ;
#4639=ORIENTED_EDGE ( 'NONE', *, *, #967, .T. ) ;
#4666=VECTOR ( 'NONE', #71, 1000.000000000000000 ) ;
#4669=DIRECTION ( 'NONE',  ( -0.000000000000000000, -0.000000000000000000, -1.000000000000000000 ) ) ;
#4671=VERTEX_POINT ( 'NONE', #5129 ) ;
#4691=VECTOR ( 'NONE', #7317, 1000.000000000000000 ) ;
#4706=EDGE_LOOP ( 'NONE', ( #1579, #1122, #2448, #4624 ) ) ;
#4713=LINE ( 'NONE', #7179, #1604 ) ;
#4715=CIRCLE ( 'NONE', #7420, 25.00000000000002132 ) ;
#4732=FACE_OUTER_BOUND ( 'NONE', #4184, .T. ) ;
#4744=DIRECTION ( 'NONE',  ( 1.000000000000000000, 0.000000000000000000, -0.000000000000000000 ) ) ;
#4757=ORIENTED_EDGE ( 'NONE', *, *, #2841, .F. ) ;
#4781=ORIENTED_EDGE ( 'NONE', *, *, #5838, .F. ) ;
#4791=FACE_OUTER_BOUND ( 'NONE', #5612, .T. ) ;
#4797=EDGE_LOOP ( 'NONE', ( #2924, #2116, #158, #7885 ) ) ;
#4809=CYLINDRICAL_SURFACE ( 'NONE', #3829, 25.00000000000000000 ) ;
#4818=CARTESIAN_POINT ( 'NONE',  ( 0.000000000000000000, 25.00000000000000000, 25.00000000000000000 ) ) ;
#4826=EDGE_CURVE ( 'NONE', #5884, #4446, #2784, .T. ) ;
#4837=VECTOR ( 'NONE', #6802, 1000.000000000000000 ) ;
#4877=ORIENTED_EDGE ( 'NONE', *, *, #4427, .F. ) ;
#4881=FACE_BOUND ( 'NONE', #2544, .T. ) ;
#4926=VERTEX_POINT ( 'NONE', #1956 ) ;
#4948=CARTESIAN_POINT ( 'NONE',  ( 362.5000000000001137, -4.592425496802566478E-15, 25.00000000000000000 ) ) ;
#4949=CARTESIAN_POINT ( 'NONE',  ( 0.000000000000000000, -25.00000000000000000, 25.00000000000000000 ) ) ;
#4991=ORIENTED_EDGE ( 'NONE', *, *, #5214, .F. ) ;
#4993=DIRECTION ( 'NONE',  ( 0.000000000000000000, 0.000000000000000000, 1.000000000000000000 ) ) ;
#5011=CYLINDRICAL_SURFACE ( 'NONE', #5013, 25.00000000000000000 ) ;
#5013=AXIS2_PLACEMENT_3D ( 'NONE', #6064, #7898, #3104 ) ;
#5042=VERTEX_POINT ( 'NONE', #6740 ) ;
#5073=ORIENTED_EDGE ( 'NONE', *, *, #6118, .T. ) ;
#5094=DIRECTION ( 'NONE',  ( -1.000000000000000000, 0.000000000000000000, 0.000000000000000000 ) ) ;
#5096=CYLINDRICAL_SURFACE ( 'NONE', #4406, 12.50000000000001066 ) ;
#5100=ORIENTED_EDGE ( 'NONE', *, *, #5326, .T. ) ;
#5112=ORIENTED_EDGE ( 'NONE', *, *, #3995, .F. ) ;
#5126=( GEOMETRIC_REPRESENTATION_CONTEXT ( 3 ) GLOBAL_UNCERTAINTY_ASSIGNED_CONTEXT ( ( #2556 ) ) GLOBAL_UNIT_ASSIGNED_CONTEXT ( ( #2962, #1626, #2318 ) ) REPRESENTATION_CONTEXT ( 'NONE', 'WORKASPACE' ) );
#5129=CARTESIAN_POINT ( 'NONE',  ( 337.5000000000000568, -6.123233995736758985E-15, 25.00000000000000000 ) ) ;
#5154=EDGE_CURVE ( 'NONE', #5578, #4446, #7542, .T. ) ;
#5180=DIRECTION ( 'NONE',  ( -0.000000000000000000, -0.000000000000000000, -1.000000000000000000 ) ) ;
#5194=CARTESIAN_POINT ( 'NONE',  ( 337.5000000000000568, -6.123233995736758985E-15, 0.000000000000000000 ) ) ;
#5210=DIRECTION ( 'NONE',  ( 1.000000000000000000, 0.000000000000000000, 0.000000000000000000 ) ) ;
#5214=EDGE_CURVE ( 'NONE', #4671, #2998, #552, .T. ) ;
#5234=DIRECTION ( 'NONE',  ( 1.000000000000000000, 0.000000000000000000, 0.000000000000000000 ) ) ;
#5259=FACE_OUTER_BOUND ( 'NONE', #3702, .T. ) ;
#5269=PRODUCT_DEFINITION_SHAPE ( 'NONE', 'NONE',  #2123 ) ;
#5276=LINE ( 'NONE', #941, #6108 ) ;
#5326=EDGE_CURVE ( 'NONE', #342, #5607, #1764, .T. ) ;
#5341=CIRCLE ( 'NONE', #1752, 12.50000000000001066 ) ;
#5356=ORIENTED_EDGE ( 'NONE', *, *, #1612, .F. ) ;
#5495=EDGE_CURVE ( 'NONE', #2143, #5042, #54, .T. ) ;
#5542=EDGE_CURVE ( 'NONE', #1637, #3100, #293, .T. ) ;
#5552=( NAMED_UNIT ( * ) PLANE_ANGLE_UNIT ( ) SI_UNIT ( $, .RADIAN. ) );
#5561=EDGE_CURVE ( 'NONE', #3167, #3644, #5761, .T. ) ;
#5578=VERTEX_POINT ( 'NONE', #3386 ) ;
#5602=CARTESIAN_POINT ( 'NONE',  ( -25.00000000000000000, 0.000000000000000000, 25.00000000000000000 ) ) ;
#5603=ORIENTED_EDGE ( 'NONE', *, *, #5154, .T. ) ;
#5607=VERTEX_POINT ( 'NONE', #3981 ) ;
#5612=EDGE_LOOP ( 'NONE', ( #3210, #1558, #1438, #4991 ) ) ;
#5620=EDGE_CURVE ( 'NONE', #5607, #7342, #4618, .T. ) ;
#5646=ORIENTED_EDGE ( 'NONE', *, *, #4321, .T. ) ;
#5652=ORIENTED_EDGE ( 'NONE', *, *, #2841, .T. ) ;
#5654=DIRECTION ( 'NONE',  ( 1.000000000000000000, 0.000000000000000000, -0.000000000000000000 ) ) ;
#5693=EDGE_CURVE ( 'NONE', #5607, #4926, #6073, .T. ) ;
#5720=CARTESIAN_POINT ( 'NONE',  ( 0.000000000000000000, 0.000000000000000000, 25.00000000000000000 ) ) ;
#5721=CARTESIAN_POINT ( 'NONE',  ( 400.0000000000000568, 25.00000000000000000, 25.00000000000000000 ) ) ;
#5760=CARTESIAN_POINT ( 'NONE',  ( 400.0000000000000568, 0.000000000000000000, 0.000000000000000000 ) ) ;
#5761=LINE ( 'NONE', #1418, #6003 ) ;
#5763=DIRECTION ( 'NONE',  ( 0.000000000000000000, 0.000000000000000000, 1.000000000000000000 ) ) ;
#5785=AXIS2_PLACEMENT_3D ( 'NONE', #4110, #4186, #2351 ) ;
#5790=DIRECTION ( 'NONE',  ( -0.000000000000000000, -0.000000000000000000, -1.000000000000000000 ) ) ;
#5803=CYLINDRICAL_SURFACE ( 'NONE', #7063, 25.00000000000002132 ) ;
#5823=CIRCLE ( 'NONE', #7106, 25.00000000000000000 ) ;
#5838=EDGE_CURVE ( 'NONE', #2143, #4671, #7661, .T. ) ;
#5844=CARTESIAN_POINT ( 'NONE',  ( 400.0000000000000568, 0.000000000000000000, 25.00000000000000000 ) ) ;
#5848=AXIS2_PLACEMENT_3D ( 'NONE', #2798, #4074, #5234 ) ;
#5884=VERTEX_POINT ( 'NONE', #6872 ) ;
#5915=DIRECTION ( 'NONE',  ( -1.000000000000000000, -0.000000000000000000, -0.000000000000000000 ) ) ;
#5953=CARTESIAN_POINT ( 'NONE',  ( 350.0000000000001137, -6.123233995736758985E-15, 25.00000000000000000 ) ) ;
#5957=EDGE_LOOP ( 'NONE', ( #2410, #719, #3154, #935, #2792 ) ) ;
#5980=CIRCLE ( 'NONE', #2397, 12.50000000000001066 ) ;
#5984=DIRECTION ( 'NONE',  ( 0.000000000000000000, 0.000000000000000000, 1.000000000000000000 ) ) ;
#5993=EDGE_LOOP ( 'NONE', ( #1948, #4781 ) ) ;
#5994=CARTESIAN_POINT ( 'NONE',  ( 350.0000000000001137, -6.123233995736758985E-15, 25.00000000000000000 ) ) ;
#5995=DIRECTION ( 'NONE',  ( 0.000000000000000000, -1.000000000000000000, 0.000000000000000000 ) ) ;
#6003=VECTOR ( 'NONE', #3869, 1000.000000000000000 ) ;
#6023=EDGE_CURVE ( 'NONE', #2998, #5042, #2942, .T. ) ;
#6064=CARTESIAN_POINT ( 'NONE',  ( 0.000000000000000000, 0.000000000000000000, 25.00000000000000000 ) ) ;
#6073=LINE ( 'NONE', #7868, #2668 ) ;
#6092=CIRCLE ( 'NONE', #2628, 25.00000000000000000 ) ;
#6108=VECTOR ( 'NONE', #4669, 1000.000000000000000 ) ;
#6111=EDGE_CURVE ( 'NONE', #7342, #6165, #806, .T. ) ;
#6115=DIRECTION ( 'NONE',  ( 1.000000000000000000, 0.000000000000000000, 0.000000000000000000 ) ) ;
#6118=EDGE_CURVE ( 'NONE', #3644, #7342, #4715, .T. ) ;
#6137=FACE_BOUND ( 'NONE', #1225, .T. ) ;
#6149=CARTESIAN_POINT ( 'NONE',  ( 400.0000000000000568, 0.000000000000000000, 25.00000000000000000 ) ) ;
#6161=CARTESIAN_POINT ( 'NONE',  ( 350.0000000000001137, -6.123233995736758985E-15, 0.000000000000000000 ) ) ;
#6165=VERTEX_POINT ( 'NONE', #2303 ) ;
#6191=FACE_OUTER_BOUND ( 'NONE', #4706, .T. ) ;
#6205=ADVANCED_FACE ( 'NONE', ( #4732 ), #4809, .T. ) ;
#6359=STYLED_ITEM('',(#7955),#4174);
#6417=DIRECTION ( 'NONE',  ( -0.000000000000000000, -0.000000000000000000, -1.000000000000000000 ) ) ;
#6427=FACE_OUTER_BOUND ( 'NONE', #1063, .T. ) ;
#6446=ADVANCED_FACE ( 'NONE', ( #3705 ), #5011, .T. ) ;
#6464=DIRECTION ( 'NONE',  ( -1.000000000000000000, 0.000000000000000000, 0.000000000000000000 ) ) ;
#6647=CARTESIAN_POINT ( 'NONE',  ( 0.000000000000000000, -25.00000000000000000, 0.000000000000000000 ) ) ;
#6663=ORIENTED_EDGE ( 'NONE', *, *, #6023, .T. ) ;
#6725=DIRECTION ( 'NONE',  ( 0.000000000000000000, 1.000000000000000000, 0.000000000000000000 ) ) ;
#6740=CARTESIAN_POINT ( 'NONE',  ( 362.5000000000001137, -4.592425496802567267E-15, 0.000000000000000000 ) ) ;
#6749=AXIS2_PLACEMENT_3D ( 'NONE', #5720, #3757, #4464 ) ;
#6752=CYLINDRICAL_SURFACE ( 'NONE', #1242, 12.50000000000001066 ) ;
#6769=AXIS2_PLACEMENT_3D ( 'NONE', #4045, #3967, #3456 ) ;
#6778=PLANE ( 'NONE',  #1599 ) ;
#6779=ORIENTED_EDGE ( 'NONE', *, *, #5326, .F. ) ;
#6802=DIRECTION ( 'NONE',  ( -0.000000000000000000, -0.000000000000000000, -1.000000000000000000 ) ) ;
#6818=ORIENTED_EDGE ( 'NONE', *, *, #7432, .T. ) ;
#6853=ORIENTED_EDGE ( 'NONE', *, *, #5561, .T. ) ;
#6861=AXIS2_PLACEMENT_3D ( 'NONE', #1707, #7256, #4154 ) ;
#6871=DIRECTION ( 'NONE',  ( -1.000000000000000000, 0.000000000000000000, 0.000000000000000000 ) ) ;
#6872=CARTESIAN_POINT ( 'NONE',  ( 387.5000000000000568, 0.000000000000000000, 0.000000000000000000 ) ) ;
#6956=( LENGTH_UNIT ( ) NAMED_UNIT ( * ) SI_UNIT ( .MILLI., .METRE. ) );
#6987=CARTESIAN_POINT ( 'NONE',  ( 400.0000000000000568, 0.000000000000000000, 25.00000000000000000 ) ) ;
#6988=CARTESIAN_POINT ( 'NONE',  ( 400.0000000000000568, 0.000000000000000000, 0.000000000000000000 ) ) ;
#7026=VECTOR ( 'NONE', #2706, 1000.000000000000000 ) ;
#7031=CARTESIAN_POINT ( 'NONE',  ( 362.5000000000001137, -4.592425496802567267E-15, 25.00000000000000000 ) ) ;
#7063=AXIS2_PLACEMENT_3D ( 'NONE', #5844, #1546, #299 ) ;
#7086=ORIENTED_EDGE ( 'NONE', *, *, #4218, .F. ) ;
#7106=AXIS2_PLACEMENT_3D ( 'NONE', #2815, #3413, #2168 ) ;
#7162=DIRECTION ( 'NONE',  ( 1.000000000000000000, 0.000000000000000000, 0.000000000000000000 ) ) ;
#7164=VECTOR ( 'NONE', #4535, 1000.000000000000000 ) ;
#7179=CARTESIAN_POINT ( 'NONE',  ( 0.000000000000000000, -25.00000000000000000, 25.00000000000000000 ) ) ;
#7210=EDGE_LOOP ( 'NONE', ( #7086, #799, #4639, #4237 ) ) ;
#7214=CYLINDRICAL_SURFACE ( 'NONE', #6861, 12.50000000000001066 ) ;
#7234=AXIS2_PLACEMENT_3D ( 'NONE', #7447, #5763, #2023 ) ;
#7237=DIRECTION ( 'NONE',  ( 1.000000000000000000, 0.000000000000000000, 0.000000000000000000 ) ) ;
#7256=DIRECTION ( 'NONE',  ( -0.000000000000000000, -0.000000000000000000, -1.000000000000000000 ) ) ;
#7279=FACE_BOUND ( 'NONE', #357, .T. ) ;
#7281=ORIENTED_EDGE ( 'NONE', *, *, #2491, .T. ) ;
#7317=DIRECTION ( 'NONE',  ( -0.000000000000000000, -0.000000000000000000, -1.000000000000000000 ) ) ;
#7342=VERTEX_POINT ( 'NONE', #3071 ) ;
#7354=PRODUCT_CONTEXT ( 'NONE', #1921, 'mechanical' ) ;
#7420=AXIS2_PLACEMENT_3D ( 'NONE', #6988, #1533, #3974 ) ;
#7432=EDGE_CURVE ( 'NONE', #4376, #5578, #2306, .T. ) ;
#7447=CARTESIAN_POINT ( 'NONE',  ( 400.0000000000000568, 0.000000000000000000, 25.00000000000000000 ) ) ;
#7537=DIRECTION ( 'NONE',  ( 0.000000000000000000, 0.000000000000000000, 1.000000000000000000 ) ) ;
#7542=LINE ( 'NONE', #245, #1253 ) ;
#7661=CIRCLE ( 'NONE', #3824, 12.50000000000001066 ) ;
#7704=PRODUCT ( 'Handle', 'Handle', '', ( #7354 ) ) ;
#7756=VECTOR ( 'NONE', #4394, 1000.000000000000000 ) ;
#7786=AXIS2_PLACEMENT_3D ( 'NONE', #6987, #4610, #5094 ) ;
#7799=DIRECTION ( 'NONE',  ( 0.000000000000000000, 0.000000000000000000, 1.000000000000000000 ) ) ;
#7802=CARTESIAN_POINT ( 'NONE',  ( 0.000000000000000000, 0.000000000000000000, 25.00000000000000000 ) ) ;
#7832=ADVANCED_FACE ( 'NONE', ( #2028 ), #5803, .T. ) ;
#7841=SHAPE_REPRESENTATION_RELATIONSHIP ( 'NONE' , 'NONE' ,  #3730, #10 ) ;
#7868=CARTESIAN_POINT ( 'NONE',  ( 0.000000000000000000, 25.00000000000000000, 25.00000000000000000 ) ) ;
#7885=ORIENTED_EDGE ( 'NONE', *, *, #4321, .F. ) ;
#7898=DIRECTION ( 'NONE',  ( -0.000000000000000000, -0.000000000000000000, -1.000000000000000000 ) ) ;
#7949=COLOUR_RGB('Sky Blue',0.24,0.69,0.87);
#7950=FILL_AREA_STYLE_COLOUR('',#7949);
#7951=FILL_AREA_STYLE('',(#7950));
#7952=SURFACE_STYLE_FILL_AREA(#7951);
#7953=SURFACE_SIDE_STYLE('',(#7952));
#7954=SURFACE_STYLE_USAGE(.BOTH.,#7953);
#7955=PRESENTATION_STYLE_ASSIGNMENT((#7954));
ENDSEC;
END-ISO-10303-21;
